ISO-10303-21;
HEADER;
/* Generated by software containing ST-Developer
 * from STEP Tools, Inc. (www.steptools.com) 
 */

FILE_DESCRIPTION(
/* description */ ('Flywheel Crank-Slider'),
/* implementation_level */ '2;1');

FILE_NAME(
/* name */ 'Flat Washer - M5.step',
/* time_stamp */ '2026-10-28T03:23:13-07:00',
/* author */ (''),
/* organization */ (''),
/* preprocessor_version */ 'ST-DEVELOPER v20.2',
/* originating_system */ 'Autodesk Translation Framework v15.17.0.0',
/* authorisation */ '');

FILE_SCHEMA (('AUTOMOTIVE_DESIGN { 1 0 10303 214 3 1 1 }'));
ENDSEC;

DATA;
#10=MECHANICAL_DESIGN_GEOMETRIC_PRESENTATION_REPRESENTATION('',(#686),#17322);
#541=CONICAL_SURFACE('',#10116,0.275,0.785398163397449);
#581=SHAPE_REPRESENTATION_RELATIONSHIP('SRR','None',#17578,#633);
#633=ADVANCED_BREP_SHAPE_REPRESENTATION('',(#745),#17282);
#686=STYLED_ITEM('',(#17938),#745);
#745=MANIFOLD_SOLID_BREP('Body1',#9066);
#904=FACE_BOUND('',#2210,.T.);
#905=FACE_BOUND('',#2213,.T.);
#1149=PLANE('',#10121);
#1150=PLANE('',#10125);
#1553=FACE_OUTER_BOUND('',#2207,.T.);
#1554=FACE_OUTER_BOUND('',#2208,.T.);
#1555=FACE_OUTER_BOUND('',#2209,.T.);
#1556=FACE_OUTER_BOUND('',#2211,.T.);
#1557=FACE_OUTER_BOUND('',#2212,.T.);
#2207=EDGE_LOOP('',(#7128,#7129,#7130,#7131));
#2208=EDGE_LOOP('',(#7132,#7133,#7134,#7135));
#2209=EDGE_LOOP('',(#7136));
#2210=EDGE_LOOP('',(#7137));
#2211=EDGE_LOOP('',(#7138,#7139,#7140,#7141));
#2212=EDGE_LOOP('',(#7142));
#2213=EDGE_LOOP('',(#7143));
#2920=LINE('',#15237,#3531);
#2921=LINE('',#15241,#3532);
#2922=LINE('',#15248,#3533);
#3531=VECTOR('',#12000,0.275);
#3532=VECTOR('',#12005,0.265);
#3533=VECTOR('',#12014,0.5);
#4013=CIRCLE('',#10117,0.285);
#4014=CIRCLE('',#10118,0.265);
#4015=CIRCLE('',#10120,0.265);
#4016=CIRCLE('',#10122,0.5);
#4017=CIRCLE('',#10124,0.5);
#4612=VERTEX_POINT('',#15234);
#4613=VERTEX_POINT('',#15236);
#4614=VERTEX_POINT('',#15240);
#4615=VERTEX_POINT('',#15244);
#4616=VERTEX_POINT('',#15247);
#5521=EDGE_CURVE('',#4612,#4612,#4013,.T.);
#5522=EDGE_CURVE('',#4612,#4613,#2920,.T.);
#5523=EDGE_CURVE('',#4613,#4613,#4014,.T.);
#5524=EDGE_CURVE('',#4613,#4614,#2921,.T.);
#5525=EDGE_CURVE('',#4614,#4614,#4015,.T.);
#5526=EDGE_CURVE('',#4615,#4615,#4016,.T.);
#5527=EDGE_CURVE('',#4615,#4616,#2922,.T.);
#5528=EDGE_CURVE('',#4616,#4616,#4017,.T.);
#7128=ORIENTED_EDGE('',*,*,#5521,.T.);
#7129=ORIENTED_EDGE('',*,*,#5522,.T.);
#7130=ORIENTED_EDGE('',*,*,#5523,.T.);
#7131=ORIENTED_EDGE('',*,*,#5522,.F.);
#7132=ORIENTED_EDGE('',*,*,#5523,.F.);
#7133=ORIENTED_EDGE('',*,*,#5524,.T.);
#7134=ORIENTED_EDGE('',*,*,#5525,.T.);
#7135=ORIENTED_EDGE('',*,*,#5524,.F.);
#7136=ORIENTED_EDGE('',*,*,#5526,.T.);
#7137=ORIENTED_EDGE('',*,*,#5521,.F.);
#7138=ORIENTED_EDGE('',*,*,#5526,.F.);
#7139=ORIENTED_EDGE('',*,*,#5527,.T.);
#7140=ORIENTED_EDGE('',*,*,#5528,.T.);
#7141=ORIENTED_EDGE('',*,*,#5527,.F.);
#7142=ORIENTED_EDGE('',*,*,#5528,.F.);
#7143=ORIENTED_EDGE('',*,*,#5525,.F.);
#8416=CYLINDRICAL_SURFACE('',#10119,0.265);
#8417=CYLINDRICAL_SURFACE('',#10123,0.5);
#8744=ADVANCED_FACE('',(#1553),#541,.F.);
#8745=ADVANCED_FACE('',(#1554),#8416,.F.);
#8746=ADVANCED_FACE('',(#1555,#904),#1149,.T.);
#8747=ADVANCED_FACE('',(#1556),#8417,.T.);
#8748=ADVANCED_FACE('',(#1557,#905),#1150,.F.);
#9066=CLOSED_SHELL('',(#8744,#8745,#8746,#8747,#8748));
#10115=AXIS2_PLACEMENT_3D('',#15232,#11994,#11995);
#10116=AXIS2_PLACEMENT_3D('',#15233,#11996,#11997);
#10117=AXIS2_PLACEMENT_3D('',#15235,#11998,#11999);
#10118=AXIS2_PLACEMENT_3D('',#15238,#12001,#12002);
#10119=AXIS2_PLACEMENT_3D('',#15239,#12003,#12004);
#10120=AXIS2_PLACEMENT_3D('',#15242,#12006,#12007);
#10121=AXIS2_PLACEMENT_3D('',#15243,#12008,#12009);
#10122=AXIS2_PLACEMENT_3D('',#15245,#12010,#12011);
#10123=AXIS2_PLACEMENT_3D('',#15246,#12012,#12013);
#10124=AXIS2_PLACEMENT_3D('',#15249,#12015,#12016);
#10125=AXIS2_PLACEMENT_3D('',#15250,#12017,#12018);
#11994=DIRECTION('axis',(0.,0.,1.));
#11995=DIRECTION('refdir',(1.,0.,0.));
#11996=DIRECTION('center_axis',(0.,1.,0.));
#11997=DIRECTION('ref_axis',(1.,0.,0.));
#11998=DIRECTION('center_axis',(0.,1.,0.));
#11999=DIRECTION('ref_axis',(1.,0.,0.));
#12000=DIRECTION('',(0.707106781186548,-0.707106781186547,-8.65956056235494E-17));
#12001=DIRECTION('center_axis',(0.,-1.,0.));
#12002=DIRECTION('ref_axis',(1.,0.,0.));
#12003=DIRECTION('center_axis',(0.,1.,0.));
#12004=DIRECTION('ref_axis',(1.,0.,0.));
#12005=DIRECTION('',(0.,-1.,0.));
#12006=DIRECTION('center_axis',(0.,-1.,0.));
#12007=DIRECTION('ref_axis',(1.,0.,0.));
#12008=DIRECTION('center_axis',(0.,1.,0.));
#12009=DIRECTION('ref_axis',(1.,0.,0.));
#12010=DIRECTION('center_axis',(0.,1.,0.));
#12011=DIRECTION('ref_axis',(1.,0.,0.));
#12012=DIRECTION('center_axis',(0.,1.,0.));
#12013=DIRECTION('ref_axis',(1.,0.,0.));
#12014=DIRECTION('',(0.,-1.,0.));
#12015=DIRECTION('center_axis',(0.,1.,0.));
#12016=DIRECTION('ref_axis',(1.,0.,0.));
#12017=DIRECTION('center_axis',(0.,1.,0.));
#12018=DIRECTION('ref_axis',(1.,0.,0.));
#15232=CARTESIAN_POINT('',(0.,0.,0.));
#15233=CARTESIAN_POINT('Origin',(0.,0.09,0.));
#15234=CARTESIAN_POINT('',(-0.285,0.1,3.49024337756996E-17));
#15235=CARTESIAN_POINT('Origin',(0.,0.1,0.));
#15236=CARTESIAN_POINT('',(-0.265,0.08,-3.24531401774049E-17));
#15237=CARTESIAN_POINT('',(-0.275,0.09,3.36777869765522E-17));
#15238=CARTESIAN_POINT('Origin',(0.,0.08,0.));
#15239=CARTESIAN_POINT('Origin',(0.,0.,0.));
#15240=CARTESIAN_POINT('',(-0.265,0.,3.24531401774049E-17));
#15241=CARTESIAN_POINT('',(-0.265,0.,3.24531401774049E-17));
#15242=CARTESIAN_POINT('Origin',(0.,0.,0.));
#15243=CARTESIAN_POINT('Origin',(0.,0.1,0.));
#15244=CARTESIAN_POINT('',(-0.5,0.1,6.12323399573677E-17));
#15245=CARTESIAN_POINT('Origin',(0.,0.1,0.));
#15246=CARTESIAN_POINT('Origin',(0.,0.,0.));
#15247=CARTESIAN_POINT('',(-0.5,0.,6.12323399573677E-17));
#15248=CARTESIAN_POINT('',(-0.5,0.,6.12323399573677E-17));
#15249=CARTESIAN_POINT('Origin',(0.,0.,0.));
#15250=CARTESIAN_POINT('Origin',(0.,0.,0.));
#17221=UNCERTAINTY_MEASURE_WITH_UNIT(LENGTH_MEASURE(0.001),#17323,
'DISTANCE_ACCURACY_VALUE',
'Maximum model space distance between geometric entities at asserted c
onnectivities');
#17261=UNCERTAINTY_MEASURE_WITH_UNIT(LENGTH_MEASURE(0.001),#17323,
'DISTANCE_ACCURACY_VALUE',
'Maximum model space distance between geometric entities at asserted c
onnectivities');
#17282=(
GEOMETRIC_REPRESENTATION_CONTEXT(3)
GLOBAL_UNCERTAINTY_ASSIGNED_CONTEXT((#17221))
GLOBAL_UNIT_ASSIGNED_CONTEXT((#17323,#17325,#17326))
REPRESENTATION_CONTEXT('','3D')
);
#17322=(
GEOMETRIC_REPRESENTATION_CONTEXT(3)
GLOBAL_UNCERTAINTY_ASSIGNED_CONTEXT((#17261))
GLOBAL_UNIT_ASSIGNED_CONTEXT((#17323,#17325,#17326))
REPRESENTATION_CONTEXT('','3D')
);
#17323=(
LENGTH_UNIT()
NAMED_UNIT(*)
SI_UNIT(.CENTI.,.METRE.)
);
#17325=(
NAMED_UNIT(*)
PLANE_ANGLE_UNIT()
SI_UNIT($,.RADIAN.)
);
#17326=(
NAMED_UNIT(*)
SI_UNIT($,.STERADIAN.)
SOLID_ANGLE_UNIT()
);
#17347=SHAPE_DEFINITION_REPRESENTATION(#17409,#17578);
#17409=PRODUCT_DEFINITION_SHAPE('',$,#17639);
#17578=SHAPE_REPRESENTATION('',(#10115),#17282);
#17618=PRODUCT_DEFINITION_CONTEXT('part definition',#17800,'design');
#17639=PRODUCT_DEFINITION('Flat Washer - M5','Flat Washer - M5',#17699,
#17618);
#17699=PRODUCT_DEFINITION_FORMATION('',$,#17822);
#17800=APPLICATION_CONTEXT(
'Core Data for Automotive Mechanical Design Process');
#17801=PRODUCT_CONTEXT('part definition',#17800,'mechanical');
#17822=PRODUCT('Flat Washer - M5','Flat Washer - M5','Flat Washer - M5',
(#17801));
#17932=COLOUR_RGB('Black',0.12,0.14,0.17);
#17933=FILL_AREA_STYLE_COLOUR('',#17932);
#17934=FILL_AREA_STYLE('',(#17933));
#17935=SURFACE_STYLE_FILL_AREA(#17934);
#17936=SURFACE_SIDE_STYLE('',(#17935));
#17937=SURFACE_STYLE_USAGE(.BOTH.,#17936);
#17938=PRESENTATION_STYLE_ASSIGNMENT((#17937));
ENDSEC;
END-ISO-10303-21;
